ISO-10303-21;
HEADER;
/* Generated by software containing ST-Developer
 * from STEP Tools, Inc. (www.steptools.com) 
 */

FILE_DESCRIPTION(
/* description */ ('Bin tilter linkage'),
/* implementation_level */ '2;1');

FILE_NAME(
/* name */ 'Pivot spacer 5 mm (1).step',
/* time_stamp */ '2026-10-28T03:26:24-07:00',
/* author */ (''),
/* organization */ (''),
/* preprocessor_version */ 'ST-DEVELOPER v20.2',
/* originating_system */ 'Autodesk Translation Framework v15.17.0.0',
/* authorisation */ '');

FILE_SCHEMA (('AUTOMOTIVE_DESIGN { 1 0 10303 214 3 1 1 }'));
ENDSEC;

DATA;
#10=MECHANICAL_DESIGN_GEOMETRIC_PRESENTATION_REPRESENTATION('',(#873),#23728);
#661=SHAPE_REPRESENTATION_RELATIONSHIP('SRR','None',#24125,#767);
#767=ADVANCED_BREP_SHAPE_REPRESENTATION('',(#987),#23625);
#873=STYLED_ITEM('',(#24779),#987);
#987=MANIFOLD_SOLID_BREP('Body1',#12403);
#1169=FACE_BOUND('',#2858,.T.);
#1170=FACE_BOUND('',#2860,.T.);
#1548=PLANE('',#13902);
#1549=PLANE('',#13903);
#1996=FACE_OUTER_BOUND('',#2855,.T.);
#1997=FACE_OUTER_BOUND('',#2856,.T.);
#1998=FACE_OUTER_BOUND('',#2857,.T.);
#1999=FACE_OUTER_BOUND('',#2859,.T.);
#2855=EDGE_LOOP('',(#8841,#8842,#8843,#8844));
#2856=EDGE_LOOP('',(#8845,#8846,#8847,#8848));
#2857=EDGE_LOOP('',(#8849));
#2858=EDGE_LOOP('',(#8850));
#2859=EDGE_LOOP('',(#8851));
#2860=EDGE_LOOP('',(#8852));
#3983=LINE('',#20259,#4658);
#3984=LINE('',#20265,#4659);
#4658=VECTOR('',#16052,0.605);
#4659=VECTOR('',#16059,0.800000000000001);
#5299=CIRCLE('',#13897,0.605);
#5300=CIRCLE('',#13898,0.605);
#5301=CIRCLE('',#13900,0.800000000000001);
#5302=CIRCLE('',#13901,0.800000000000001);
#6113=VERTEX_POINT('',#20256);
#6114=VERTEX_POINT('',#20258);
#6115=VERTEX_POINT('',#20262);
#6116=VERTEX_POINT('',#20264);
#7160=EDGE_CURVE('',#6113,#6113,#5299,.T.);
#7161=EDGE_CURVE('',#6113,#6114,#3983,.T.);
#7162=EDGE_CURVE('',#6114,#6114,#5300,.T.);
#7163=EDGE_CURVE('',#6115,#6115,#5301,.T.);
#7164=EDGE_CURVE('',#6115,#6116,#3984,.T.);
#7165=EDGE_CURVE('',#6116,#6116,#5302,.T.);
#8841=ORIENTED_EDGE('',*,*,#7160,.F.);
#8842=ORIENTED_EDGE('',*,*,#7161,.T.);
#8843=ORIENTED_EDGE('',*,*,#7162,.T.);
#8844=ORIENTED_EDGE('',*,*,#7161,.F.);
#8845=ORIENTED_EDGE('',*,*,#7163,.F.);
#8846=ORIENTED_EDGE('',*,*,#7164,.T.);
#8847=ORIENTED_EDGE('',*,*,#7165,.T.);
#8848=ORIENTED_EDGE('',*,*,#7164,.F.);
#8849=ORIENTED_EDGE('',*,*,#7163,.T.);
#8850=ORIENTED_EDGE('',*,*,#7160,.T.);
#8851=ORIENTED_EDGE('',*,*,#7165,.F.);
#8852=ORIENTED_EDGE('',*,*,#7162,.F.);
#11317=CYLINDRICAL_SURFACE('',#13896,0.605);
#11318=CYLINDRICAL_SURFACE('',#13899,0.800000000000001);
#11721=ADVANCED_FACE('',(#1996),#11317,.F.);
#11722=ADVANCED_FACE('',(#1997),#11318,.T.);
#11723=ADVANCED_FACE('',(#1998,#1169),#1548,.T.);
#11724=ADVANCED_FACE('',(#1999,#1170),#1549,.F.);
#12403=CLOSED_SHELL('',(#11721,#11722,#11723,#11724));
#13895=AXIS2_PLACEMENT_3D('',#20254,#16046,#16047);
#13896=AXIS2_PLACEMENT_3D('',#20255,#16048,#16049);
#13897=AXIS2_PLACEMENT_3D('',#20257,#16050,#16051);
#13898=AXIS2_PLACEMENT_3D('',#20260,#16053,#16054);
#13899=AXIS2_PLACEMENT_3D('',#20261,#16055,#16056);
#13900=AXIS2_PLACEMENT_3D('',#20263,#16057,#16058);
#13901=AXIS2_PLACEMENT_3D('',#20266,#16060,#16061);
#13902=AXIS2_PLACEMENT_3D('',#20267,#16062,#16063);
#13903=AXIS2_PLACEMENT_3D('',#20268,#16064,#16065);
#16046=DIRECTION('axis',(0.,0.,1.));
#16047=DIRECTION('refdir',(1.,0.,0.));
#16048=DIRECTION('center_axis',(0.,1.,0.));
#16049=DIRECTION('ref_axis',(1.,0.,0.));
#16050=DIRECTION('center_axis',(0.,-1.,0.));
#16051=DIRECTION('ref_axis',(1.,0.,0.));
#16052=DIRECTION('',(0.,-1.,0.));
#16053=DIRECTION('center_axis',(0.,-1.,0.));
#16054=DIRECTION('ref_axis',(1.,0.,0.));
#16055=DIRECTION('center_axis',(0.,1.,0.));
#16056=DIRECTION('ref_axis',(1.,0.,0.));
#16057=DIRECTION('center_axis',(0.,1.,0.));
#16058=DIRECTION('ref_axis',(1.,0.,0.));
#16059=DIRECTION('',(0.,-1.,0.));
#16060=DIRECTION('center_axis',(0.,1.,0.));
#16061=DIRECTION('ref_axis',(1.,0.,0.));
#16062=DIRECTION('center_axis',(0.,1.,0.));
#16063=DIRECTION('ref_axis',(1.,0.,0.));
#16064=DIRECTION('center_axis',(0.,1.,0.));
#16065=DIRECTION('ref_axis',(1.,0.,0.));
#20254=CARTESIAN_POINT('',(0.,0.,0.));
#20255=CARTESIAN_POINT('Origin',(18.,-1.,15.));
#20256=CARTESIAN_POINT('',(17.395,-0.5,15.));
#20257=CARTESIAN_POINT('Origin',(18.,-0.5,15.));
#20258=CARTESIAN_POINT('',(17.395,-1.,15.));
#20259=CARTESIAN_POINT('',(17.395,-1.,15.));
#20260=CARTESIAN_POINT('Origin',(18.,-1.,15.));
#20261=CARTESIAN_POINT('Origin',(18.,-1.,15.));
#20262=CARTESIAN_POINT('',(17.2,-0.5,15.));
#20263=CARTESIAN_POINT('Origin',(18.,-0.5,15.));
#20264=CARTESIAN_POINT('',(17.2,-1.,15.));
#20265=CARTESIAN_POINT('',(17.2,-1.,15.));
#20266=CARTESIAN_POINT('Origin',(18.,-1.,15.));
#20267=CARTESIAN_POINT('Origin',(18.,-0.5,15.));
#20268=CARTESIAN_POINT('Origin',(18.,-1.,15.));
#23508=UNCERTAINTY_MEASURE_WITH_UNIT(LENGTH_MEASURE(0.001),#23729,
'DISTANCE_ACCURACY_VALUE',
'Maximum model space distance between geometric entities at asserted c
onnectivities');
#23611=UNCERTAINTY_MEASURE_WITH_UNIT(LENGTH_MEASURE(0.001),#23729,
'DISTANCE_ACCURACY_VALUE',
'Maximum model space distance between geometric entities at asserted c
onnectivities');
#23625=(
GEOMETRIC_REPRESENTATION_CONTEXT(3)
GLOBAL_UNCERTAINTY_ASSIGNED_CONTEXT((#23508))
GLOBAL_UNIT_ASSIGNED_CONTEXT((#23729,#23731,#23732))
REPRESENTATION_CONTEXT('','3D')
);
#23728=(
GEOMETRIC_REPRESENTATION_CONTEXT(3)
GLOBAL_UNCERTAINTY_ASSIGNED_CONTEXT((#23611))
GLOBAL_UNIT_ASSIGNED_CONTEXT((#23729,#23731,#23732))
REPRESENTATION_CONTEXT('','3D')
);
#23729=(
LENGTH_UNIT()
NAMED_UNIT(*)
SI_UNIT(.CENTI.,.METRE.)
);
#23731=(
NAMED_UNIT(*)
PLANE_ANGLE_UNIT()
SI_UNIT($,.RADIAN.)
);
#23732=(
NAMED_UNIT(*)
SI_UNIT($,.STERADIAN.)
SOLID_ANGLE_UNIT()
);
#23746=SHAPE_DEFINITION_REPRESENTATION(#23862,#24125);
#23862=PRODUCT_DEFINITION_SHAPE('',$,#24242);
#24125=SHAPE_REPRESENTATION('',(#13895),#23625);
#24228=PRODUCT_DEFINITION_CONTEXT('part definition',#24578,'design');
#24242=PRODUCT_DEFINITION('Pivot spacer 5 mm (1)','Pivot spacer 5 mm (1)',
#24358,#24228);
#24358=PRODUCT_DEFINITION_FORMATION('',$,#24593);
#24578=APPLICATION_CONTEXT(
'Core Data for Automotive Mechanical Design Process');
#24579=PRODUCT_CONTEXT('part definition',#24578,'mechanical');
#24593=PRODUCT('Pivot spacer 5 mm (1)','Pivot spacer 5 mm (1)',
'Pivot spacer 5 mm (1)',(#24579));
#24773=COLOUR_RGB('Off White',0.89,0.88,0.83);
#24774=FILL_AREA_STYLE_COLOUR('',#24773);
#24775=FILL_AREA_STYLE('',(#24774));
#24776=SURFACE_STYLE_FILL_AREA(#24775);
#24777=SURFACE_SIDE_STYLE('',(#24776));
#24778=SURFACE_STYLE_USAGE(.BOTH.,#24777);
#24779=PRESENTATION_STYLE_ASSIGNMENT((#24778));
ENDSEC;
END-ISO-10303-21;
